ISO-10303-21;
HEADER;
FILE_DESCRIPTION (('STEP AP214'),
    '1' );
FILE_NAME ('machine screw nut hex_ai_MSHXNUT 0.375-16-S-N.step',
    '2026-10-08T05:56:58',
    ( '' ),
    ( '' ),
    'SwSTEP 2.0',
    'SolidWorks 2026',
    '' );
FILE_SCHEMA (( 'AUTOMOTIVE_DESIGN' ));
ENDSEC;

DATA;
#23=CARTESIAN_POINT ( 'NONE',  ( -5.313169144388804277, -6.097875887622428159, -0.08160424337824753738 ) ) ;
#36=SURFACE_STYLE_FILL_AREA ( #16650 ) ;
#69=ORIENTED_EDGE ( 'NONE', *, *, #7451, .F. ) ;
#149=DIRECTION ( 'NONE',  ( 1.000000000000000000, 0.000000000000000000, -0.000000000000000000 ) ) ;
#153=CARTESIAN_POINT ( 'NONE',  ( 1.545624935189822177E-15, 9.165435523385314198, -6.527800000000000047 ) ) ;
#179=VECTOR ( 'NONE', #5539, 1000.000000000000000 ) ;
#201=VERTEX_POINT ( 'NONE', #5838 ) ;
#246=FACE_OUTER_BOUND ( 'NONE', #2374, .T. ) ;
#260=AXIS2_PLACEMENT_3D ( 'NONE', #9213, #397, #16916 ) ;
#294=( LENGTH_UNIT ( ) NAMED_UNIT ( * ) SI_UNIT ( .MILLI., .METRE. ) );
#314=DIRECTION ( 'NONE',  ( 0.000000000000000000, 0.000000000000000000, -1.000000000000000000 ) ) ;
#364=ORIENTED_EDGE ( 'NONE', *, *, #11679, .T. ) ;
#366=ORIENTED_EDGE ( 'NONE', *, *, #9892, .F. ) ;
#368=ADVANCED_FACE ( 'NONE', ( #12448 ), #16395, .F. ) ;
#370=CARTESIAN_POINT ( 'NONE',  ( 0.000000000000000000, 0.000000000000000000, -6.527800000000000047 ) ) ;
#380=B_SPLINE_CURVE_WITH_KNOTS ( 'NONE', 3,
 ( #13281, #8977, #18084, #2664, #14786, #5762 ),
 .UNSPECIFIED., .F., .F.,
 ( 4, 2, 4 ),
 ( 2.380731676443570881E-07, 0.002318718087522258532, 0.004637198101876872751 ),
 .UNSPECIFIED. ) ;
#397=DIRECTION ( 'NONE',  ( 0.5000000000000004441, -0.8660254037844383745, 0.000000000000000000 ) ) ;
#422=ORIENTED_EDGE ( 'NONE', *, *, #14453, .F. ) ;
#426=B_SPLINE_CURVE_WITH_KNOTS ( 'NONE', 3,
 ( #7792, #796, #17497, #14401, #5671, #2568 ),
 .UNSPECIFIED., .F., .F.,
 ( 4, 2, 4 ),
 ( 0.008176170726434979844, 0.01049421029328160074, 0.01281224986012821990 ),
 .UNSPECIFIED. ) ;
#475=DIRECTION ( 'NONE',  ( -0.000000000000000000, -0.000000000000000000, -1.000000000000000000 ) ) ;
#489=DIRECTION ( 'NONE',  ( 0.8660254037844380415, -0.5000000000000009992, 0.000000000000000000 ) ) ;
#550=LINE ( 'NONE', #6821, #5143 ) ;
#558=ORIENTED_EDGE ( 'NONE', *, *, #6224, .F. ) ;
#590=FACE_OUTER_BOUND ( 'NONE', #15857, .T. ) ;
#614=ORIENTED_EDGE ( 'NONE', *, *, #4205, .T. ) ;
#657=CARTESIAN_POINT ( 'NONE',  ( 7.288264926088301010, -4.957553806382933637, -0.4925372136696608560 ) ) ;
#679=ADVANCED_FACE ( 'NONE', ( #2109 ), #5546, .F. ) ;
#699=DIRECTION ( 'NONE',  ( 0.000000000000000000, 0.000000000000000000, 1.000000000000000000 ) ) ;
#748=CARTESIAN_POINT ( 'NONE',  ( -7.937500000000000000, -1.543790678740078581, -0.06656457167770332695 ) ) ;
#765=MECHANICAL_DESIGN_GEOMETRIC_PRESENTATION_REPRESENTATION('',(#9068),#11313);
#796=CARTESIAN_POINT ( 'NONE',  ( 7.937499999999998224, -3.837375845242625871, -0.4937872269236130429 ) ) ;
#820=ORIENTED_EDGE ( 'NONE', *, *, #2202, .T. ) ;
#835=ORIENTED_EDGE ( 'NONE', *, *, #7451, .T. ) ;
#860=ORIENTED_EDGE ( 'NONE', *, *, #16548, .F. ) ;
#883=EDGE_CURVE ( 'NONE', #1239, #4468, #19601, .T. ) ;
#931=CARTESIAN_POINT ( 'NONE',  ( 1.734723475976807094E-15, 9.165435523385314198, -0.7089489049740167470 ) ) ;
#954=EDGE_CURVE ( 'NONE', #8718, #1239, #7054, .T. ) ;
#956=CARTESIAN_POINT ( 'NONE',  ( 0.000000000000000000, 0.000000000000000000, 0.000000000000000000 ) ) ;
#1005=ORIENTED_EDGE ( 'NONE', *, *, #11824, .F. ) ;
#1021=CARTESIAN_POINT ( 'NONE',  ( 2.624839991567102793, 7.649983447674348902, -0.06756670027993921801 ) ) ;
#1043=FACE_OUTER_BOUND ( 'NONE', #16772, .T. ) ;
#1181=FACE_OUTER_BOUND ( 'NONE', #3715, .T. ) ;
#1189=CIRCLE ( 'NONE', #19389, 7.937500000000000000 ) ;
#1210=CARTESIAN_POINT ( 'NONE',  ( -0.6476140635210462237, 8.791535369480451223, -0.4930775504667659903 ) ) ;
#1215=VERTEX_POINT ( 'NONE', #19085 ) ;
#1237=EDGE_CURVE ( 'NONE', #8660, #11518, #6111, .T. ) ;
#1239=VERTEX_POINT ( 'NONE', #14691 ) ;
#1264=VERTEX_POINT ( 'NONE', #5570 ) ;
#1303=EDGE_CURVE ( 'NONE', #1215, #9544, #380, .T. ) ;
#1435=DIRECTION ( 'NONE',  ( 1.000000000000000000, 0.000000000000000000, 0.000000000000000000 ) ) ;
#1451=AXIS2_PLACEMENT_3D ( 'NONE', #13087, #8391, #16198 ) ;
#1454=EDGE_LOOP ( 'NONE', ( #10584, #364, #3636 ) ) ;
#1465=ORIENTED_EDGE ( 'NONE', *, *, #13603, .F. ) ;
#1490=ADVANCED_FACE ( 'NONE', ( #5236 ), #12273, .T. ) ;
#1505=DIRECTION ( 'NONE',  ( -1.000000000000000000, 0.000000000000000000, 0.000000000000000000 ) ) ;
#1531=EDGE_LOOP ( 'NONE', ( #3319, #9054, #19673, #4040, #1858 ) ) ;
#1542=( NAMED_UNIT ( * ) SI_UNIT ( $, .STERADIAN. ) SOLID_ANGLE_UNIT ( ) );
#1577=ORIENTED_EDGE ( 'NONE', *, *, #11824, .T. ) ;
#1580=CONICAL_SURFACE ( 'NONE', #9252, 7.937500000000000000, 1.047197551196596521 ) ;
#1641=LINE ( 'NONE', #9249, #4189 ) ;
#1684=AXIS2_PLACEMENT_3D ( 'NONE', #370, #11478, #6555 ) ;
#1694=CARTESIAN_POINT ( 'NONE',  ( 7.937500000000000000, 3.841717848563049209, -0.4950406553165793144 ) ) ;
#1750=DIRECTION ( 'NONE',  ( 0.000000000000000000, 0.000000000000000000, 1.000000000000000000 ) ) ;
#1760=EDGE_CURVE ( 'NONE', #5856, #8313, #3514, .T. ) ;
#1836=ORIENTED_EDGE ( 'NONE', *, *, #12753, .T. ) ;
#1844=ORIENTED_EDGE ( 'NONE', *, *, #16931, .F. ) ;
#1858=ORIENTED_EDGE ( 'NONE', *, *, #2864, .T. ) ;
#1869=CARTESIAN_POINT ( 'NONE',  ( 0.000000000000000000, 0.000000000000000000, 0.000000000000000000 ) ) ;
#1967=ORIENTED_EDGE ( 'NONE', *, *, #1237, .T. ) ;
#2095=DIRECTION ( 'NONE',  ( 1.000000000000000000, 0.000000000000000000, 0.000000000000000000 ) ) ;
#2109=FACE_OUTER_BOUND ( 'NONE', #2867, .T. ) ;
#2187=ORIENTED_EDGE ( 'NONE', *, *, #6685, .F. ) ;
#2202=EDGE_CURVE ( 'NONE', #16599, #5161, #426, .T. ) ;
#2216=DIRECTION ( 'NONE',  ( 0.000000000000000000, 0.000000000000000000, 1.000000000000000000 ) ) ;
#2233=CIRCLE ( 'NONE', #11507, 4.762500000000000178 ) ;
#2349=DIRECTION ( 'NONE',  ( -0.000000000000000000, -0.000000000000000000, -1.000000000000000000 ) ) ;
#2374=EDGE_LOOP ( 'NONE', ( #18650, #10854, #1844, #12183, #11255 ) ) ;
#2378=CARTESIAN_POINT ( 'NONE',  ( 4.305564957446062380, 6.679616436190405793, 4.844604941820970789E-15 ) ) ;
#2421=ORIENTED_EDGE ( 'NONE', *, *, #6751, .T. ) ;
#2448=ADVANCED_FACE ( 'NONE', ( #1181 ), #9347, .F. ) ;
#2463=ORIENTED_EDGE ( 'NONE', *, *, #13603, .T. ) ;
#2502=VERTEX_POINT ( 'NONE', #3471 ) ;
#2547=EDGE_CURVE ( 'NONE', #9544, #8660, #7419, .T. ) ;
#2563=AXIS2_PLACEMENT_3D ( 'NONE', #18503, #7690, #1505 ) ;
#2568=CARTESIAN_POINT ( 'NONE',  ( 7.937500000000000000, 0.000000000000000000, 0.000000000000000000 ) ) ;
#2588=SHAPE_REPRESENTATION ( 'machine screw nut hex_ai_MSHXNUT 0.375-16-S-N', ( #16724 ), #5229 ) ;
#2602=CARTESIAN_POINT ( 'NONE',  ( 1.734723475976807094E-15, 9.165435523385314198, -0.7089489049740167470 ) ) ;
#2656=ORIENTED_EDGE ( 'NONE', *, *, #954, .F. ) ;
#2664=CARTESIAN_POINT ( 'NONE',  ( -5.312660008432906977, 6.098169837403609961, -0.06756670027994018946 ) ) ;
#2708=ORIENTED_EDGE ( 'NONE', *, *, #16548, .T. ) ;
#2836=AXIS2_PLACEMENT_3D ( 'NONE', #19340, #16345, #11745 ) ;
#2864=EDGE_CURVE ( 'NONE', #6786, #11375, #13861, .T. ) ;
#2867=EDGE_LOOP ( 'NONE', ( #6580, #7697, #16472, #2187 ) ) ;
#2916=CARTESIAN_POINT ( 'NONE',  ( -7.289885936478958328, -4.956617915597525403, -0.4930775504667679332 ) ) ;
#2920=EDGE_CURVE ( 'NONE', #3846, #1264, #10961, .T. ) ;
#2953=DIRECTION ( 'NONE',  ( -0.000000000000000000, -0.000000000000000000, 1.000000000000000000 ) ) ;
#2966=ADVANCED_FACE ( 'NONE', ( #13144 ), #17459, .F. ) ;
#3040=AXIS2_PLACEMENT_3D ( 'NONE', #3783, #14505, #9999 ) ;
#3072=VECTOR ( 'NONE', #3207, 1000.000000000000000 ) ;
#3080=CARTESIAN_POINT ( 'NONE',  ( -2.602085213965210642E-14, -9.165435523385315975, -0.7089489049740167470 ) ) ;
#3096=FACE_OUTER_BOUND ( 'NONE', #17023, .T. ) ;
#3111=CARTESIAN_POINT ( 'NONE',  ( -1.001543065824775120E-15, -9.165435523385328409, -6.527800000000000047 ) ) ;
#3181=CARTESIAN_POINT ( 'NONE',  ( -15.87499999999998579, -1.734723475976807094E-15, -6.527800000000000047 ) ) ;
#3185=CARTESIAN_POINT ( 'NONE',  ( 7.937500000000000000, 0.000000000000000000, 0.000000000000000000 ) ) ;
#3201=CYLINDRICAL_SURFACE ( 'NONE', #13164, 4.762500000000000178 ) ;
#3207=DIRECTION ( 'NONE',  ( 0.000000000000000000, 0.000000000000000000, 1.000000000000000000 ) ) ;
#3286=CARTESIAN_POINT ( 'NONE',  ( 7.937500000000001776, 0.7748640365313755884, -6.324512672832110842E-17 ) ) ;
#3316=DIRECTION ( 'NONE',  ( -0.000000000000000000, -0.000000000000000000, 1.000000000000000000 ) ) ;
#3319=ORIENTED_EDGE ( 'NONE', *, *, #11844, .T. ) ;
#3447=FACE_BOUND ( 'NONE', #14696, .T. ) ;
#3471=CARTESIAN_POINT ( 'NONE',  ( -3.968750000000000000, 4.860316984116057109E-16, -0.5557897334539606549 ) ) ;
#3514=LINE ( 'NONE', #12429, #18350 ) ;
#3589=( NAMED_UNIT ( * ) PLANE_ANGLE_UNIT ( ) SI_UNIT ( $, .RADIAN. ) );
#3597=ADVANCED_FACE ( 'NONE', ( #5509 ), #11433, .T. ) ;
#3618=VERTEX_POINT ( 'NONE', #17822 ) ;
#3636=ORIENTED_EDGE ( 'NONE', *, *, #1303, .F. ) ;
#3649=CARTESIAN_POINT ( 'NONE',  ( 3.968750000000004441, -6.874076642538978987, 0.000000000000000000 ) ) ;
#3715=EDGE_LOOP ( 'NONE', ( #17033, #2708, #10778, #8562 ) ) ;
#3727=CARTESIAN_POINT ( 'NONE',  ( -7.937500000000000000, 0.000000000000000000, 0.000000000000000000 ) ) ;
#3754=CARTESIAN_POINT ( 'NONE',  ( 3.968750000000004441, -6.874076642538978987, 0.000000000000000000 ) ) ;
#3783=CARTESIAN_POINT ( 'NONE',  ( 0.000000000000000000, 0.000000000000000000, -0.6113687067993561763 ) ) ;
#3803=CARTESIAN_POINT ( 'NONE',  ( -3.968750000000004441, 6.874076642538978987, 0.000000000000000000 ) ) ;
#3834=AXIS2_PLACEMENT_3D ( 'NONE', #19529, #4524, #13336 ) ;
#3846=VERTEX_POINT ( 'NONE', #9610 ) ;
#3901=DIRECTION ( 'NONE',  ( -1.000000000000000000, 0.000000000000000000, 0.000000000000000000 ) ) ;
#3995=CARTESIAN_POINT ( 'NONE',  ( 3.293609449816393475, -7.263869220928335757, -0.01675691374233746408 ) ) ;
#4019=CIRCLE ( 'NONE', #10097, 7.937500000000000000 ) ;
#4040=ORIENTED_EDGE ( 'NONE', *, *, #12523, .F. ) ;
#4088=VERTEX_POINT ( 'NONE', #3754 ) ;
#4143=CARTESIAN_POINT ( 'NONE',  ( 0.000000000000000000, 0.000000000000000000, 0.000000000000000000 ) ) ;
#4184=CARTESIAN_POINT ( 'NONE',  ( 4.762500000000000178, 0.000000000000000000, -25.03750572909317285 ) ) ;
#4189=VECTOR ( 'NONE', #10654, 1000.000000000000000 ) ;
#4205=EDGE_CURVE ( 'NONE', #5161, #4088, #15908, .T. ) ;
#4288=CARTESIAN_POINT ( 'NONE',  ( -2.602085213965210642E-14, -9.165435523385315975, -0.7089489049740167470 ) ) ;
#4303=( NAMED_UNIT ( * ) PLANE_ANGLE_UNIT ( ) SI_UNIT ( $, .RADIAN. ) );
#4333=DIRECTION ( 'NONE',  ( 0.000000000000000000, 0.000000000000000000, 1.000000000000000000 ) ) ;
#4401=SURFACE_SIDE_STYLE ('',( #12009 ) ) ;
#4431=CYLINDRICAL_SURFACE ( 'NONE', #3834, 3.968750000000000000 ) ;
#4468=VERTEX_POINT ( 'NONE', #3727 ) ;
#4492=CARTESIAN_POINT ( 'NONE',  ( -1.303212546021025764, -8.413025409128790599, -0.3142460757452265052 ) ) ;
#4504=EDGE_LOOP ( 'NONE', ( #12554, #11362, #5384, #7813, #5435 ) ) ;
#4522=CARTESIAN_POINT ( 'NONE',  ( -4.643890550183624732, -6.484284064149645310, -0.01675691374233593753 ) ) ;
#4524=DIRECTION ( 'NONE',  ( 0.000000000000000000, 0.000000000000000000, 1.000000000000000000 ) ) ;
#4536=FILL_AREA_STYLE_COLOUR ( '', #7810 ) ;
#4537=AXIS2_PLACEMENT_3D ( 'NONE', #19774, #13478, #6067 ) ;
#4586=VERTEX_POINT ( 'NONE', #11817 ) ;
#4593=B_SPLINE_CURVE_WITH_KNOTS ( 'NONE', 3,
 ( #3185, #3286, #9298, #15400, #1694, #18493 ),
 .UNSPECIFIED., .F., .F.,
 ( 4, 2, 4 ),
 ( 0.01281224986012821990, 0.01513166665602956075, 0.01745108345193090160 ),
 .UNSPECIFIED. ) ;
#4628=CARTESIAN_POINT ( 'NONE',  ( -4.305564957446068597, -6.679616436190415563, -1.463672932855429408E-15 ) ) ;
#4645=DIRECTION ( 'NONE',  ( 0.000000000000000000, 0.000000000000000000, 1.000000000000000000 ) ) ;
#4695=CARTESIAN_POINT ( 'NONE',  ( -7.937500000000000000, 3.090998114436792843, -0.3168978725525089524 ) ) ;
#4702=CARTESIAN_POINT ( 'NONE',  ( 1.734723475976807094E-15, 9.165435523385314198, -0.7089489049740167470 ) ) ;
#4768=ORIENTED_EDGE ( 'NONE', *, *, #7722, .F. ) ;
#4789=VECTOR ( 'NONE', #9942, 1000.000000000000114 ) ;
#4862=AXIS2_PLACEMENT_3D ( 'NONE', #3181, #18297, #18393 ) ;
#4884=AXIS2_PLACEMENT_3D ( 'NONE', #8455, #9963, #16056 ) ;
#5010=DIRECTION ( 'NONE',  ( 1.000000000000000000, 0.000000000000000000, 0.000000000000000000 ) ) ;
#5054=VERTEX_POINT ( 'NONE', #18881 ) ;
#5063=CARTESIAN_POINT ( 'NONE',  ( 0.000000000000000000, 0.000000000000000000, 0.000000000000000000 ) ) ;
#5068=CIRCLE ( 'NONE', #11148, 4.762500000000000178 ) ;
#5084=SHAPE_REPRESENTATION_RELATIONSHIP ( 'NONE' , 'NONE' ,  #2588, #19745 ) ;
#5108=ORIENTED_EDGE ( 'NONE', *, *, #18398, .F. ) ;
#5143=VECTOR ( 'NONE', #12552, 1000.000000000000000 ) ;
#5152=DIRECTION ( 'NONE',  ( 0.000000000000000000, 0.000000000000000000, -1.000000000000000000 ) ) ;
#5154=VERTEX_POINT ( 'NONE', #11573 ) ;
#5161=VERTEX_POINT ( 'NONE', #16279 ) ;
#5164=AXIS2_PLACEMENT_3D ( 'NONE', #6591, #3316, #5010 ) ;
#5203=DIRECTION ( 'NONE',  ( 0.000000000000000000, 0.000000000000000000, -1.000000000000000000 ) ) ;
#5219=CARTESIAN_POINT ( 'NONE',  ( -3.889375000000000693, 4.763110644433737781E-16, -0.6113687067993561763 ) ) ;
#5229=( GEOMETRIC_REPRESENTATION_CONTEXT ( 3 ) GLOBAL_UNCERTAINTY_ASSIGNED_CONTEXT ( ( #11990 ) ) GLOBAL_UNIT_ASSIGNED_CONTEXT ( ( #18020, #4303, #7688 ) ) REPRESENTATION_CONTEXT ( 'NONE', 'WORKASPACE' ) );
#5236=FACE_OUTER_BOUND ( 'NONE', #19658, .T. ) ;
#5357=ORIENTED_EDGE ( 'NONE', *, *, #12753, .F. ) ;
#5384=ORIENTED_EDGE ( 'NONE', *, *, #18760, .T. ) ;
#5413=CARTESIAN_POINT ( 'NONE',  ( -2.624330855611205937, 7.650277397455539585, -0.08160424337824208341 ) ) ;
#5435=ORIENTED_EDGE ( 'NONE', *, *, #14453, .T. ) ;
#5453=DIRECTION ( 'NONE',  ( -0.000000000000000000, -0.000000000000000000, 1.000000000000000000 ) ) ;
#5482=CARTESIAN_POINT ( 'NONE',  ( 1.300631254478300303, -8.414515718495838570, -0.3148715423363500632 ) ) ;
#5509=FACE_OUTER_BOUND ( 'NONE', #4504, .T. ) ;
#5525=CONICAL_SURFACE ( 'NONE', #10967, 7.937500000000000000, 1.047197551196596521 ) ;
#5526=CARTESIAN_POINT ( 'NONE',  ( -7.937499999999998224, -3.837375845242624095, -0.4937872269236123768 ) ) ;
#5532=DIRECTION ( 'NONE',  ( 1.000000000000000000, 0.000000000000000000, 0.000000000000000000 ) ) ;
#5536=ORIENTED_EDGE ( 'NONE', *, *, #883, .F. ) ;
#5539=DIRECTION ( 'NONE',  ( 0.000000000000000000, 0.000000000000000000, 1.000000000000000000 ) ) ;
#5546=CONICAL_SURFACE ( 'NONE', #19271, 4.762500000000000178, 0.9599310885968813656 ) ;
#5570=CARTESIAN_POINT ( 'NONE',  ( -4.762499999999999289, 5.832380380939268136E-16, 0.000000000000000000 ) ) ;
#5625=ORIENTED_EDGE ( 'NONE', *, *, #14312, .F. ) ;
#5648=VECTOR ( 'NONE', #11175, 1000.000000000000227 ) ;
#5671=CARTESIAN_POINT ( 'NONE',  ( 7.937500000000000000, -0.7744039358429353204, 6.268043809681820044E-17 ) ) ;
#5678=CARTESIAN_POINT ( 'NONE',  ( -3.968750000000000000, 4.860316984116057109E-16, -6.527800000000000047 ) ) ;
#5731=EDGE_CURVE ( 'NONE', #8313, #8718, #16530, .T. ) ;
#5757=CARTESIAN_POINT ( 'NONE',  ( 3.968750000000000000, 0.000000000000000000, -6.527800000000000047 ) ) ;
#5762=CARTESIAN_POINT ( 'NONE',  ( -3.968750000000004441, 6.874076642538978987, 0.000000000000000000 ) ) ;
#5822=FACE_OUTER_BOUND ( 'NONE', #18098, .T. ) ;
#5827=DIRECTION ( 'NONE',  ( -0.000000000000000000, -0.000000000000000000, -1.000000000000000000 ) ) ;
#5838=CARTESIAN_POINT ( 'NONE',  ( -3.968750000000000000, 4.860316984116057109E-16, -5.946610266546040968 ) ) ;
#5856=VERTEX_POINT ( 'NONE', #6688 ) ;
#5868=ORIENTED_EDGE ( 'NONE', *, *, #1760, .T. ) ;
#5983=CARTESIAN_POINT ( 'NONE',  ( -7.937499999999998224, 0.7748640365313737011, -6.860966872759830281E-17 ) ) ;
#6030=AXIS2_PLACEMENT_3D ( 'NONE', #11468, #11561, #17762 ) ;
#6067=DIRECTION ( 'NONE',  ( 1.000000000000000000, 0.000000000000000000, 0.000000000000000000 ) ) ;
#6075=PLANE ( 'NONE',  #4862 ) ;
#6086=SURFACE_STYLE_USAGE ( .BOTH. , #4401 ) ;
#6111=B_SPLINE_CURVE_WITH_KNOTS ( 'NONE', 3,
 ( #19179, #2378, #11584, #7057, #16288, #11489, #12894, #11680 ),
 .UNSPECIFIED., .F., .F.,
 ( 4, 2, 2, 4 ),
 ( 0.004637198101876887496, 0.005792104118025196563, 0.006947010134173506497, 0.009256822166470123764 ),
 .UNSPECIFIED. ) ;
#6151=ORIENTED_EDGE ( 'NONE', *, *, #10432, .F. ) ;
#6224=EDGE_CURVE ( 'NONE', #8313, #9186, #15497, .T. ) ;
#6230=DIRECTION ( 'NONE',  ( 1.000000000000000000, 0.000000000000000000, 0.000000000000000000 ) ) ;
#6232=DIRECTION ( 'NONE',  ( 0.000000000000000000, 0.000000000000000000, 1.000000000000000000 ) ) ;
#6236=DIRECTION ( 'NONE',  ( -0.8660254037844382635, -0.5000000000000005551, 0.000000000000000000 ) ) ;
#6272=DIRECTION ( 'NONE',  ( 0.8660254037844382635, 0.5000000000000005551, 0.000000000000000000 ) ) ;
#6331=ORIENTED_EDGE ( 'NONE', *, *, #9263, .F. ) ;
#6384=VECTOR ( 'NONE', #8792, 1000.000000000000000 ) ;
#6419=LINE ( 'NONE', #15457, #18826 ) ;
#6431=ORIENTED_EDGE ( 'NONE', *, *, #7510, .F. ) ;
#6492=B_SPLINE_CURVE_WITH_KNOTS ( 'NONE', 3,
 ( #17362, #657, #9566, #8352, #14564, #3649 ),
 .UNSPECIFIED., .F., .F.,
 ( 4, 2, 4 ),
 ( 2.380731676487269046E-07, 0.002318718087522257665, 0.004637198101876866679 ),
 .UNSPECIFIED. ) ;
#6526=FACE_OUTER_BOUND ( 'NONE', #16957, .T. ) ;
#6555=DIRECTION ( 'NONE',  ( 1.000000000000000000, 0.000000000000000000, 0.000000000000000000 ) ) ;
#6580=ORIENTED_EDGE ( 'NONE', *, *, #11742, .F. ) ;
#6591=CARTESIAN_POINT ( 'NONE',  ( 0.000000000000000000, 0.000000000000000000, 0.000000000000000000 ) ) ;
#6640=PRODUCT_DEFINITION_SHAPE ( 'NONE', 'NONE',  #16784 ) ;
#6685=EDGE_CURVE ( 'NONE', #7112, #5154, #13791, .T. ) ;
#6688=CARTESIAN_POINT ( 'NONE',  ( -7.937500000000000000, -4.582717761692662428, -6.527800000000000047 ) ) ;
#6751=EDGE_CURVE ( 'NONE', #15630, #3846, #10353, .T. ) ;
#6786=VERTEX_POINT ( 'NONE', #19530 ) ;
#6821=CARTESIAN_POINT ( 'NONE',  ( 7.937500000000000000, 4.582717761692648217, -6.527800000000000047 ) ) ;
#6824=CARTESIAN_POINT ( 'NONE',  ( -7.937500000000000000, 0.000000000000000000, 0.000000000000000000 ) ) ;
#6825=CARTESIAN_POINT ( 'NONE',  ( 0.000000000000000000, 0.000000000000000000, 0.000000000000000000 ) ) ;
#6917=AXIS2_PLACEMENT_3D ( 'NONE', #9943, #17725, #19028 ) ;
#6987=B_SPLINE_CURVE_WITH_KNOTS ( 'NONE', 3,
 ( #16028, #13030, #19123, #5413, #17627, #14820, #1210, #2602 ),
 .UNSPECIFIED., .F., .F.,
 ( 4, 2, 2, 4 ),
 ( 0.004637198101876872751, 0.005792104118025187022, 0.006947010134173500426, 0.009256822166470130703 ),
 .UNSPECIFIED. ) ;
#7032=VERTEX_POINT ( 'NONE', #7290 ) ;
#7051=CARTESIAN_POINT ( 'NONE',  ( 0.000000000000000000, 0.000000000000000000, -0.5557897334539606549 ) ) ;
#7054=B_SPLINE_CURVE_WITH_KNOTS ( 'NONE', 3,
 ( #10509, #8903, #4492, #10603, #13798, #12201 ),
 .UNSPECIFIED., .F., .F.,
 ( 4, 2, 4 ),
 ( 2.380731676726218893E-07, 0.002318718087522284119, 0.004637198101876895302 ),
 .UNSPECIFIED. ) ;
#7057=CARTESIAN_POINT ( 'NONE',  ( 5.313169144388799836, 6.097875887622421054, -0.08160424337823990459 ) ) ;
#7076=FACE_OUTER_BOUND ( 'NONE', #18119, .T. ) ;
#7112=VERTEX_POINT ( 'NONE', #14922 ) ;
#7120=AXIS2_PLACEMENT_3D ( 'NONE', #8312, #19202, #8606 ) ;
#7124=CARTESIAN_POINT ( 'NONE',  ( 7.937500000000000000, 4.582717761692648217, -6.527800000000000047 ) ) ;
#7125=CARTESIAN_POINT ( 'NONE',  ( 0.000000000000000000, 0.000000000000000000, 0.000000000000000000 ) ) ;
#7143=ADVANCED_FACE ( 'NONE', ( #18319 ), #3201, .F. ) ;
#7167=LINE ( 'NONE', #5678, #12867 ) ;
#7187=EDGE_LOOP ( 'NONE', ( #17805, #6151, #11116, #558, #9557, #422 ) ) ;
#7248=DIRECTION ( 'NONE',  ( 1.000000000000000000, 0.000000000000000000, 0.000000000000000000 ) ) ;
#7285=ORIENTED_EDGE ( 'NONE', *, *, #16385, .F. ) ;
#7290=CARTESIAN_POINT ( 'NONE',  ( 7.937500000000000000, 4.582717761692648217, -6.527800000000000047 ) ) ;
#7298=CARTESIAN_POINT ( 'NONE',  ( 3.968750000000007994, 6.874076642538976323, 0.000000000000000000 ) ) ;
#7333=FACE_OUTER_BOUND ( 'NONE', #1454, .T. ) ;
#7411=CARTESIAN_POINT ( 'NONE',  ( 1.545624935189822177E-15, 9.165435523385314198, -6.527800000000000047 ) ) ;
#7419=CIRCLE ( 'NONE', #12566, 7.937500000000000000 ) ;
#7451=EDGE_CURVE ( 'NONE', #4088, #8718, #13321, .T. ) ;
#7510=EDGE_CURVE ( 'NONE', #201, #2502, #7167, .T. ) ;
#7525=SURFACE_STYLE_USAGE ( .BOTH. , #9047 ) ;
#7600=DIRECTION ( 'NONE',  ( -0.000000000000000000, -0.000000000000000000, 1.000000000000000000 ) ) ;
#7622=CARTESIAN_POINT ( 'NONE',  ( 0.000000000000000000, 0.000000000000000000, -6.502399999999998847 ) ) ;
#7688=( NAMED_UNIT ( * ) SI_UNIT ( $, .STERADIAN. ) SOLID_ANGLE_UNIT ( ) );
#7690=DIRECTION ( 'NONE',  ( 0.000000000000000000, 0.000000000000000000, -1.000000000000000000 ) ) ;
#7697=ORIENTED_EDGE ( 'NONE', *, *, #9263, .T. ) ;
#7722=EDGE_CURVE ( 'NONE', #4586, #3618, #10314, .T. ) ;
#7741=CARTESIAN_POINT ( 'NONE',  ( 7.937500000000000000, 4.582717761692648217, -6.527800000000000047 ) ) ;
#7768=EDGE_LOOP ( 'NONE', ( #14109, #2656, #69 ) ) ;
#7792=CARTESIAN_POINT ( 'NONE',  ( 7.937499999999996447, -4.582717761692668645, -0.7089489049740167470 ) ) ;
#7809=ORIENTED_EDGE ( 'NONE', *, *, #16674, .F. ) ;
#7810=COLOUR_RGB ( '', 0.66274510, 0.83137255, 0.94901961) ;
#7813=ORIENTED_EDGE ( 'NONE', *, *, #11844, .F. ) ;
#7871=EDGE_LOOP ( 'NONE', ( #19739, #8895, #1836, #17867 ) ) ;
#7890=FACE_OUTER_BOUND ( 'NONE', #13575, .T. ) ;
#7950=CARTESIAN_POINT ( 'NONE',  ( 7.937500000000000000, -4.582717761692665981, -6.527800000000000047 ) ) ;
#7974=CARTESIAN_POINT ( 'NONE',  ( -1.001543065824775120E-15, -9.165435523385328409, -6.527800000000000047 ) ) ;
#8032=DIRECTION ( 'NONE',  ( -0.8660254037844380415, 0.5000000000000009992, 0.000000000000000000 ) ) ;
#8050=ORIENTED_EDGE ( 'NONE', *, *, #18223, .F. ) ;
#8125=AXIS2_PLACEMENT_3D ( 'NONE', #6825, #12951, #15284 ) ;
#8213=ORIENTED_EDGE ( 'NONE', *, *, #5731, .T. ) ;
#8312=CARTESIAN_POINT ( 'NONE',  ( 0.000000000000000000, 0.000000000000000000, 0.000000000000000000 ) ) ;
#8313=VERTEX_POINT ( 'NONE', #18126 ) ;
#8352=CARTESIAN_POINT ( 'NONE',  ( 5.312660008432906977, -6.098169837403623283, -0.06756670027994693406 ) ) ;
#8391=DIRECTION ( 'NONE',  ( -0.000000000000000000, -0.000000000000000000, 1.000000000000000000 ) ) ;
#8404=VECTOR ( 'NONE', #6236, 1000.000000000000114 ) ;
#8412=ORIENTED_EDGE ( 'NONE', *, *, #2920, .F. ) ;
#8455=CARTESIAN_POINT ( 'NONE',  ( 0.000000000000000000, 0.000000000000000000, 0.000000000000000000 ) ) ;
#8468=MECHANICAL_DESIGN_GEOMETRIC_PRESENTATION_REPRESENTATION('',(#11019),#18373);
#8562=ORIENTED_EDGE ( 'NONE', *, *, #6751, .F. ) ;
#8606=DIRECTION ( 'NONE',  ( 1.000000000000000000, 1.776356839400250465E-15, 0.000000000000000000 ) ) ;
#8660=VERTEX_POINT ( 'NONE', #16996 ) ;
#8712=ADVANCED_FACE ( 'NONE', ( #9097, #12590 ), #6075, .F. ) ;
#8718=VERTEX_POINT ( 'NONE', #3080 ) ;
#8724=AXIS2_PLACEMENT_3D ( 'NONE', #19239, #11455, #5532 ) ;
#8753=LINE ( 'NONE', #8855, #16330 ) ;
#8792=DIRECTION ( 'NONE',  ( 0.000000000000000000, -1.000000000000000000, 0.000000000000000000 ) ) ;
#8805=CARTESIAN_POINT ( 'NONE',  ( -7.937500000000000000, 1.560264056424245815, -0.06840592591720176530 ) ) ;
#8842=DIRECTION ( 'NONE',  ( 0.8191520442889898002, 0.000000000000000000, 0.5735764363510488240 ) ) ;
#8855=CARTESIAN_POINT ( 'NONE',  ( -4.762500000000000178, 0.000000000000000000, -6.502399999999998847 ) ) ;
#8892=CARTESIAN_POINT ( 'NONE',  ( 3.631935042553954940, -7.068536848887564616, -2.426114119173129746E-15 ) ) ;
#8895=ORIENTED_EDGE ( 'NONE', *, *, #7722, .T. ) ;
#8903=CARTESIAN_POINT ( 'NONE',  ( -0.6492350739117196401, -8.790599478695048319, -0.4925372136696601344 ) ) ;
#8906=FILL_AREA_STYLE_COLOUR ( '', #19597 ) ;
#8939=DIRECTION ( 'NONE',  ( -0.000000000000000000, -0.000000000000000000, -1.000000000000000000 ) ) ;
#8940=CARTESIAN_POINT ( 'NONE',  ( 3.889375000000000693, 0.000000000000000000, -0.6113687067993561763 ) ) ;
#8977=CARTESIAN_POINT ( 'NONE',  ( -7.288264926088305451, 4.957553806382917649, -0.4925372136696566372 ) ) ;
#9006=PRESENTATION_STYLE_ASSIGNMENT (( #6086 ) ) ;
#9047=SURFACE_SIDE_STYLE ('',( #36 ) ) ;
#9054=ORIENTED_EDGE ( 'NONE', *, *, #1303, .T. ) ;
#9068=STYLED_ITEM ( 'NONE', ( #9006 ), #19745 ) ;
#9077=ORIENTED_EDGE ( 'NONE', *, *, #10170, .F. ) ;
#9097=FACE_BOUND ( 'NONE', #19257, .T. ) ;
#9135=CARTESIAN_POINT ( 'NONE',  ( -6.636868745521697477, -5.333637566582153156, -0.3148715423363437904 ) ) ;
#9139=DIRECTION ( 'NONE',  ( -0.5000000000000004441, 0.8660254037844383745, 0.000000000000000000 ) ) ;
#9148=( NAMED_UNIT ( * ) PLANE_ANGLE_UNIT ( ) SI_UNIT ( $, .RADIAN. ) );
#9166=CARTESIAN_POINT ( 'NONE',  ( 0.000000000000000000, 0.000000000000000000, -25.03750572909317285 ) ) ;
#9182=EDGE_LOOP ( 'NONE', ( #860, #9283, #2421, #14678 ) ) ;
#9186=VERTEX_POINT ( 'NONE', #7950 ) ;
#9213=CARTESIAN_POINT ( 'NONE',  ( -1.001543065824775120E-15, -9.165435523385328409, -6.527800000000000047 ) ) ;
#9249=CARTESIAN_POINT ( 'NONE',  ( -4.762500000000000178, 5.832380380939270108E-16, -25.03750572909317285 ) ) ;
#9252=AXIS2_PLACEMENT_3D ( 'NONE', #18171, #13453, #19554 ) ;
#9263=EDGE_CURVE ( 'NONE', #18451, #201, #19643, .T. ) ;
#9283=ORIENTED_EDGE ( 'NONE', *, *, #9892, .T. ) ;
#9298=CARTESIAN_POINT ( 'NONE',  ( 7.937500000000001776, 1.560264056424248258, -0.06840592591720123794 ) ) ;
#9346=( LENGTH_UNIT ( ) NAMED_UNIT ( * ) SI_UNIT ( .MILLI., .METRE. ) );
#9347=CONICAL_SURFACE ( 'NONE', #4537, 3.889375000000000693, 0.9599310885968779239 ) ;
#9358=CARTESIAN_POINT ( 'NONE',  ( -15.87499999999998579, -1.734723475976807094E-15, 0.000000000000000000 ) ) ;
#9360=SHAPE_DEFINITION_REPRESENTATION ( #6640, #2588 ) ;
#9397=MANIFOLD_SOLID_BREP ( 'EndChamfer', #19571 ) ;
#9437=ORIENTED_EDGE ( 'NONE', *, *, #19437, .F. ) ;
#9457=LINE ( 'NONE', #7741, #19668 ) ;
#9544=VERTEX_POINT ( 'NONE', #3803 ) ;
#9557=ORIENTED_EDGE ( 'NONE', *, *, #1760, .F. ) ;
#9566=CARTESIAN_POINT ( 'NONE',  ( 6.634287453978997107, -5.335127875949193132, -0.3142460757452261721 ) ) ;
#9601=CARTESIAN_POINT ( 'NONE',  ( -7.937500000000000000, 4.582717761692651770, -6.527800000000000047 ) ) ;
#9610=CARTESIAN_POINT ( 'NONE',  ( 4.762499999999999289, 0.000000000000000000, 0.000000000000000000 ) ) ;
#9685=LINE ( 'NONE', #18769, #5648 ) ;
#9701=DIRECTION ( 'NONE',  ( -0.5000000000000009992, -0.8660254037844380415, 0.000000000000000000 ) ) ;
#9714=ADVANCED_FACE ( 'NONE', ( #590 ), #15893, .T. ) ;
#9743=EDGE_LOOP ( 'NONE', ( #15561, #18754, #2463, #5357 ) ) ;
#9792=AXIS2_PLACEMENT_3D ( 'NONE', #7124, #16346, #19440 ) ;
#9833=DIRECTION ( 'NONE',  ( 0.000000000000000000, 0.000000000000000000, 1.000000000000000000 ) ) ;
#9844=LINE ( 'NONE', #15933, #17578 ) ;
#9892=EDGE_CURVE ( 'NONE', #2502, #15630, #19334, .T. ) ;
#9910=B_SPLINE_CURVE_WITH_KNOTS ( 'NONE', 3,
 ( #19232, #5526, #11634, #748, #17737, #6824 ),
 .UNSPECIFIED., .F., .F.,
 ( 4, 2, 4 ),
 ( 0.008176170726434978109, 0.01049421029328159553, 0.01281224986012821296 ),
 .UNSPECIFIED. ) ;
#9931=ORIENTED_EDGE ( 'NONE', *, *, #2547, .T. ) ;
#9942=DIRECTION ( 'NONE',  ( -0.8191520442889898002, 1.003171929053522282E-16, 0.5735764363510488240 ) ) ;
#9943=CARTESIAN_POINT ( 'NONE',  ( -7.937500000000000000, 4.582717761692651770, -6.527800000000000047 ) ) ;
#9963=DIRECTION ( 'NONE',  ( -0.000000000000000000, -0.000000000000000000, 1.000000000000000000 ) ) ;
#9986=EDGE_CURVE ( 'NONE', #18451, #15630, #14881, .T. ) ;
#9990=ORIENTED_EDGE ( 'NONE', *, *, #7510, .T. ) ;
#9999=DIRECTION ( 'NONE',  ( 1.000000000000000000, 0.000000000000000000, 0.000000000000000000 ) ) ;
#10048=CONICAL_SURFACE ( 'NONE', #3040, 3.889375000000000693, 0.9599310885968779239 ) ;
#10097=AXIS2_PLACEMENT_3D ( 'NONE', #4143, #5827, #12146 ) ;
#10170=EDGE_CURVE ( 'NONE', #4088, #1239, #4019, .T. ) ;
#10185=ADVANCED_FACE ( 'NONE', ( #1043 ), #10447, .T. ) ;
#10196=DIRECTION ( 'NONE',  ( -0.000000000000000000, -0.000000000000000000, 1.000000000000000000 ) ) ;
#10225=LINE ( 'NONE', #5219, #4789 ) ;
#10314=CIRCLE ( 'NONE', #1684, 4.762500000000000178 ) ;
#10337=AXIS2_PLACEMENT_3D ( 'NONE', #18941, #11350, #12747 ) ;
#10353=LINE ( 'NONE', #8940, #13154 ) ;
#10354=CARTESIAN_POINT ( 'NONE',  ( 0.000000000000000000, 0.000000000000000000, -6.502399999999998847 ) ) ;
#10432=EDGE_CURVE ( 'NONE', #7032, #6786, #9457, .T. ) ;
#10447=PLANE ( 'NONE',  #9792 ) ;
#10509=CARTESIAN_POINT ( 'NONE',  ( -2.602085213965210642E-14, -9.165435523385315975, -0.7089489049740167470 ) ) ;
#10584=ORIENTED_EDGE ( 'NONE', *, *, #18760, .F. ) ;
#10587=ORIENTED_EDGE ( 'NONE', *, *, #18006, .F. ) ;
#10603=CARTESIAN_POINT ( 'NONE',  ( -2.624839991567115227, -7.649983447674356007, -0.06756670027994669814 ) ) ;
#10637=CARTESIAN_POINT ( 'NONE',  ( -5.645569974854468320, -5.905964178674223852, -0.1296323192022640625 ) ) ;
#10654=DIRECTION ( 'NONE',  ( -0.000000000000000000, -0.000000000000000000, 1.000000000000000000 ) ) ;
#10778=ORIENTED_EDGE ( 'NONE', *, *, #18398, .T. ) ;
#10854=ORIENTED_EDGE ( 'NONE', *, *, #16653, .F. ) ;
#10865=ORIENTED_EDGE ( 'NONE', *, *, #16653, .T. ) ;
#10961=CIRCLE ( 'NONE', #4884, 4.762499999999999289 ) ;
#10967=AXIS2_PLACEMENT_3D ( 'NONE', #18868, #5152, #11271 ) ;
#10986=ORIENTED_EDGE ( 'NONE', *, *, #11742, .T. ) ;
#11019=STYLED_ITEM ( 'NONE', ( #13647 ), #9397 ) ;
#11043=EDGE_LOOP ( 'NONE', ( #11854, #10986, #1465, #13194 ) ) ;
#11059=CYLINDRICAL_SURFACE ( 'NONE', #16261, 4.762500000000000178 ) ;
#11098=( NAMED_UNIT ( * ) SI_UNIT ( $, .STERADIAN. ) SOLID_ANGLE_UNIT ( ) );
#11116=ORIENTED_EDGE ( 'NONE', *, *, #16931, .T. ) ;
#11148=AXIS2_PLACEMENT_3D ( 'NONE', #10354, #16451, #2095 ) ;
#11175=DIRECTION ( 'NONE',  ( 0.8191520442889917986, 1.003171929053524747E-16, -0.5735764363510460484 ) ) ;
#11249=PLANE ( 'NONE',  #15476 ) ;
#11255=ORIENTED_EDGE ( 'NONE', *, *, #17661, .F. ) ;
#11271=DIRECTION ( 'NONE',  ( -1.000000000000000000, 0.000000000000000000, 0.000000000000000000 ) ) ;
#11313=( GEOMETRIC_REPRESENTATION_CONTEXT ( 3 ) GLOBAL_UNCERTAINTY_ASSIGNED_CONTEXT ( ( #13004 ) ) GLOBAL_UNIT_ASSIGNED_CONTEXT ( ( #294, #3589, #11098 ) ) REPRESENTATION_CONTEXT ( 'NONE', 'WORKASPACE' ) );
#11324=CARTESIAN_POINT ( 'NONE',  ( 3.968750000000000000, 0.000000000000000000, -5.946610266546040968 ) ) ;
#11350=DIRECTION ( 'NONE',  ( 0.000000000000000000, 0.000000000000000000, -1.000000000000000000 ) ) ;
#11362=ORIENTED_EDGE ( 'NONE', *, *, #14312, .T. ) ;
#11375=VERTEX_POINT ( 'NONE', #16589 ) ;
#11433=PLANE ( 'NONE',  #6917 ) ;
#11455=DIRECTION ( 'NONE',  ( 0.000000000000000000, 0.000000000000000000, 1.000000000000000000 ) ) ;
#11468=CARTESIAN_POINT ( 'NONE',  ( 0.000000000000000000, 0.000000000000000000, 0.000000000000000000 ) ) ;
#11478=DIRECTION ( 'NONE',  ( -0.000000000000000000, -0.000000000000000000, -1.000000000000000000 ) ) ;
#11486=CONICAL_SURFACE ( 'NONE', #6030, 7.937500000000000000, 1.047197551196596521 ) ;
#11489=CARTESIAN_POINT ( 'NONE',  ( 6.636868745521693924, 5.333637566582140721, -0.3148715423363380173 ) ) ;
#11507=AXIS2_PLACEMENT_3D ( 'NONE', #16745, #8939, #1435 ) ;
#11518=VERTEX_POINT ( 'NONE', #12581 ) ;
#11561=DIRECTION ( 'NONE',  ( 0.000000000000000000, 0.000000000000000000, -1.000000000000000000 ) ) ;
#11563=DIRECTION ( 'NONE',  ( 1.000000000000000000, 0.000000000000000000, 0.000000000000000000 ) ) ;
#11573=CARTESIAN_POINT ( 'NONE',  ( -4.762500000000000178, 0.000000000000000000, -6.502399999999998847 ) ) ;
#11584=CARTESIAN_POINT ( 'NONE',  ( 4.643890550183617627, 6.484284064149637317, -0.01675691374232827352 ) ) ;
#11597=CARTESIAN_POINT ( 'NONE',  ( 2.624330855611206381, -7.650277397455553796, -0.08160424337825018803 ) ) ;
#11617=CARTESIAN_POINT ( 'NONE',  ( 7.937499999999996447, -4.582717761692668645, -0.7089489049740167470 ) ) ;
#11634=CARTESIAN_POINT ( 'NONE',  ( -7.937500000000000000, -3.073999505363502749, -0.3133235625263136037 ) ) ;
#11679=EDGE_CURVE ( 'NONE', #4468, #9544, #1189, .T. ) ;
#11680=CARTESIAN_POINT ( 'NONE',  ( 7.937500000000000000, 4.582717761692664205, -0.7089489049740167470 ) ) ;
#11714=ORIENTED_EDGE ( 'NONE', *, *, #12523, .T. ) ;
#11742=EDGE_CURVE ( 'NONE', #18451, #7112, #9685, .T. ) ;
#11745=DIRECTION ( 'NONE',  ( 1.000000000000000000, 0.000000000000000000, 0.000000000000000000 ) ) ;
#11794=DIRECTION ( 'NONE',  ( 0.000000000000000000, 0.000000000000000000, 1.000000000000000000 ) ) ;
#11817=CARTESIAN_POINT ( 'NONE',  ( -4.762500000000000178, 5.832380380939270108E-16, -6.527800000000000047 ) ) ;
#11819=ORIENTED_EDGE ( 'NONE', *, *, #954, .T. ) ;
#11824=EDGE_CURVE ( 'NONE', #1239, #5054, #12477, .T. ) ;
#11838=PLANE ( 'NONE',  #19169 ) ;
#11844=EDGE_CURVE ( 'NONE', #11375, #1215, #13635, .T. ) ;
#11854=ORIENTED_EDGE ( 'NONE', *, *, #14531, .T. ) ;
#11861=AXIS2_PLACEMENT_3D ( 'NONE', #7622, #13737, #13638 ) ;
#11880=FACE_OUTER_BOUND ( 'NONE', #9182, .T. ) ;
#11967=B_SPLINE_CURVE_WITH_KNOTS ( 'NONE', 3,
 ( #931, #16148, #13324, #1021, #19040, #7298 ),
 .UNSPECIFIED., .F., .F.,
 ( 4, 2, 4 ),
 ( 2.380731676442874196E-07, 0.002318718087522266338, 0.004637198101876887496 ),
 .UNSPECIFIED. ) ;
#11990=UNCERTAINTY_MEASURE_WITH_UNIT (LENGTH_MEASURE( 1.000000000000000082E-05 ), #18020, 'distance_accuracy_value', 'NONE');
#12009=SURFACE_STYLE_FILL_AREA ( #15010 ) ;
#12139=CARTESIAN_POINT ( 'NONE',  ( -7.937500000000000000, -4.582717761692664205, -0.7089489049740167470 ) ) ;
#12146=DIRECTION ( 'NONE',  ( 1.000000000000000000, 0.000000000000000000, 0.000000000000000000 ) ) ;
#12183=ORIENTED_EDGE ( 'NONE', *, *, #18006, .T. ) ;
#12201=CARTESIAN_POINT ( 'NONE',  ( -3.968750000000007994, -6.874076642538976323, 0.000000000000000000 ) ) ;
#12273=CONICAL_SURFACE ( 'NONE', #8125, 7.937500000000000000, 1.047197551196596521 ) ;
#12277=CIRCLE ( 'NONE', #1451, 3.968750000000000000 ) ;
#12332=ORIENTED_EDGE ( 'NONE', *, *, #11679, .F. ) ;
#12423=ORIENTED_EDGE ( 'NONE', *, *, #9986, .T. ) ;
#12429=CARTESIAN_POINT ( 'NONE',  ( -7.937500000000000000, -4.582717761692662428, -6.527800000000000047 ) ) ;
#12448=FACE_OUTER_BOUND ( 'NONE', #11043, .T. ) ;
#12464=VERTEX_POINT ( 'NONE', #4702 ) ;
#12467=ADVANCED_FACE ( 'NONE', ( #7890 ), #14098, .T. ) ;
#12477=B_SPLINE_CURVE_WITH_KNOTS ( 'NONE', 3,
 ( #16639, #4628, #4522, #23, #10637, #9135, #2916, #12139 ),
 .UNSPECIFIED., .F., .F.,
 ( 4, 2, 2, 4 ),
 ( 0.004637198101876895302, 0.005792104118025203502, 0.006947010134173512569, 0.009256822166470130703 ),
 .UNSPECIFIED. ) ;
#12515=APPLICATION_CONTEXT ( 'automotive_design' ) ;
#12521=CIRCLE ( 'NONE', #5164, 4.762499999999999289 ) ;
#12523=EDGE_CURVE ( 'NONE', #6786, #12464, #14512, .T. ) ;
#12552=DIRECTION ( 'NONE',  ( 0.000000000000000000, 0.000000000000000000, 1.000000000000000000 ) ) ;
#12554=ORIENTED_EDGE ( 'NONE', *, *, #14086, .T. ) ;
#12566=AXIS2_PLACEMENT_3D ( 'NONE', #1869, #17276, #18382 ) ;
#12581=CARTESIAN_POINT ( 'NONE',  ( 7.937500000000000000, 4.582717761692664205, -0.7089489049740167470 ) ) ;
#12590=FACE_OUTER_BOUND ( 'NONE', #7187, .T. ) ;
#12657=PLANE ( 'NONE',  #12920 ) ;
#12747=DIRECTION ( 'NONE',  ( -1.000000000000000000, 0.000000000000000000, 0.000000000000000000 ) ) ;
#12753=EDGE_CURVE ( 'NONE', #3618, #7112, #13686, .T. ) ;
#12773=FACE_OUTER_BOUND ( 'NONE', #16860, .T. ) ;
#12867=VECTOR ( 'NONE', #11794, 1000.000000000000000 ) ;
#12873=DIRECTION ( 'NONE',  ( 1.000000000000000000, 1.776356839400250465E-15, 0.000000000000000000 ) ) ;
#12894=CARTESIAN_POINT ( 'NONE',  ( 7.289885936478948558, 4.956617915597515633, -0.4930775504667603837 ) ) ;
#12896=PRODUCT ( 'machine screw nut hex_ai_MSHXNUT 0.375-16-S-N', 'machine screw nut hex_ai_MSHXNUT 0.375-16-S-N', '', ( #15365 ) ) ;
#12920=AXIS2_PLACEMENT_3D ( 'NONE', #9358, #1750, #149 ) ;
#12951=DIRECTION ( 'NONE',  ( 0.000000000000000000, 0.000000000000000000, -1.000000000000000000 ) ) ;
#13004=UNCERTAINTY_MEASURE_WITH_UNIT (LENGTH_MEASURE( 1.000000000000000082E-05 ), #294, 'distance_accuracy_value', 'NONE');
#13030=CARTESIAN_POINT ( 'NONE',  ( -3.631935042553950055, 7.068536848887553958, 4.616894251167434456E-15 ) ) ;
#13087=CARTESIAN_POINT ( 'NONE',  ( 0.000000000000000000, 0.000000000000000000, -5.946610266546040968 ) ) ;
#13144=FACE_OUTER_BOUND ( 'NONE', #14966, .T. ) ;
#13154=VECTOR ( 'NONE', #8842, 1000.000000000000114 ) ;
#13164=AXIS2_PLACEMENT_3D ( 'NONE', #17115, #7600, #16828 ) ;
#13194=ORIENTED_EDGE ( 'NONE', *, *, #17807, .F. ) ;
#13259=CARTESIAN_POINT ( 'NONE',  ( 0.000000000000000000, 0.000000000000000000, -5.946610266546040968 ) ) ;
#13281=CARTESIAN_POINT ( 'NONE',  ( -7.937500000000000000, 4.582717761692651770, -0.7089489049740185234 ) ) ;
#13321=B_SPLINE_CURVE_WITH_KNOTS ( 'NONE', 3,
 ( #19590, #8892, #3995, #11597, #17698, #5482, #14896, #4288 ),
 .UNSPECIFIED., .F., .F.,
 ( 4, 2, 2, 4 ),
 ( 0.004637198101876866679, 0.005792104118025186155, 0.006947010134173505630, 0.009256822166470144581 ),
 .UNSPECIFIED. ) ;
#13324=CARTESIAN_POINT ( 'NONE',  ( 1.303212546021007334, 8.413025409128788823, -0.3142460757452215092 ) ) ;
#13336=DIRECTION ( 'NONE',  ( 1.000000000000000000, 0.000000000000000000, 0.000000000000000000 ) ) ;
#13342=DIRECTION ( 'NONE',  ( 1.000000000000000000, 0.000000000000000000, 0.000000000000000000 ) ) ;
#13345=ADVANCED_FACE ( 'NONE', ( #15563 ), #11059, .F. ) ;
#13453=DIRECTION ( 'NONE',  ( 0.000000000000000000, 0.000000000000000000, -1.000000000000000000 ) ) ;
#13470=EDGE_CURVE ( 'NONE', #16599, #4088, #6492, .T. ) ;
#13478=DIRECTION ( 'NONE',  ( -0.000000000000000000, -0.000000000000000000, 1.000000000000000000 ) ) ;
#13483=CARTESIAN_POINT ( 'NONE',  ( 7.937500000000000000, 4.582717761692648217, -6.527800000000000047 ) ) ;
#13575=EDGE_LOOP ( 'NONE', ( #10865, #18681, #835, #13770, #15071 ) ) ;
#13590=EDGE_CURVE ( 'NONE', #15630, #2502, #13699, .T. ) ;
#13603=EDGE_CURVE ( 'NONE', #5154, #7112, #5068, .T. ) ;
#13635=LINE ( 'NONE', #15243, #14928 ) ;
#13638=DIRECTION ( 'NONE',  ( 1.000000000000000000, 0.000000000000000000, 0.000000000000000000 ) ) ;
#13647=PRESENTATION_STYLE_ASSIGNMENT (( #7525 ) ) ;
#13656=ORIENTED_EDGE ( 'NONE', *, *, #4205, .F. ) ;
#13686=LINE ( 'NONE', #4184, #15280 ) ;
#13699=CIRCLE ( 'NONE', #2836, 3.968750000000000000 ) ;
#13737=DIRECTION ( 'NONE',  ( -0.000000000000000000, -0.000000000000000000, 1.000000000000000000 ) ) ;
#13764=CONICAL_SURFACE ( 'NONE', #19192, 7.937500000000000000, 1.047197551196596521 ) ;
#13770=ORIENTED_EDGE ( 'NONE', *, *, #5731, .F. ) ;
#13791=CIRCLE ( 'NONE', #11861, 4.762500000000000178 ) ;
#13798=CARTESIAN_POINT ( 'NONE',  ( -3.292592168578611034, -7.264456548524809598, -1.328147661294742734E-15 ) ) ;
#13852=ORIENTED_EDGE ( 'NONE', *, *, #14531, .F. ) ;
#13861=LINE ( 'NONE', #153, #8404 ) ;
#13890=AXIS2_PLACEMENT_3D ( 'NONE', #13259, #19250, #16259 ) ;
#13915=APPLICATION_CONTEXT ( 'automotive_design' ) ;
#14041=ADVANCED_FACE ( 'NONE', ( #19159 ), #11486, .T. ) ;
#14048=CARTESIAN_POINT ( 'NONE',  ( 7.937500000000000000, 4.582717761692648217, -6.527800000000000047 ) ) ;
#14062=ORIENTED_EDGE ( 'NONE', *, *, #13590, .F. ) ;
#14086=EDGE_CURVE ( 'NONE', #5856, #5054, #6419, .T. ) ;
#14090=LINE ( 'NONE', #9601, #16800 ) ;
#14098=PLANE ( 'NONE',  #260 ) ;
#14109=ORIENTED_EDGE ( 'NONE', *, *, #10170, .T. ) ;
#14117=DIRECTION ( 'NONE',  ( -1.000000000000000000, 0.000000000000000000, 0.000000000000000000 ) ) ;
#14220=CARTESIAN_POINT ( 'NONE',  ( 0.000000000000000000, 0.000000000000000000, -6.502399999999998847 ) ) ;
#14312=EDGE_CURVE ( 'NONE', #5054, #4468, #9910, .T. ) ;
#14399=DIRECTION ( 'NONE',  ( 0.000000000000000000, -1.000000000000000000, 0.000000000000000000 ) ) ;
#14401=CARTESIAN_POINT ( 'NONE',  ( 7.937500000000000000, -1.543790678740078581, -0.06656457167770415961 ) ) ;
#14438=ORIENTED_EDGE ( 'NONE', *, *, #19437, .T. ) ;
#14453=EDGE_CURVE ( 'NONE', #11375, #5856, #14090, .T. ) ;
#14505=DIRECTION ( 'NONE',  ( -0.000000000000000000, -0.000000000000000000, 1.000000000000000000 ) ) ;
#14512=LINE ( 'NONE', #14697, #17185 ) ;
#14531=EDGE_CURVE ( 'NONE', #201, #18451, #12277, .T. ) ;
#14564=CARTESIAN_POINT ( 'NONE',  ( 4.644907831421413391, -6.483696736553170581, -2.385244779468109755E-15 ) ) ;
#14573=ADVANCED_FACE ( 'NONE', ( #11880 ), #10048, .F. ) ;
#14678=ORIENTED_EDGE ( 'NONE', *, *, #2920, .T. ) ;
#14691=CARTESIAN_POINT ( 'NONE',  ( -3.968750000000007994, -6.874076642538976323, 0.000000000000000000 ) ) ;
#14696=EDGE_LOOP ( 'NONE', ( #8412, #5108 ) ) ;
#14697=CARTESIAN_POINT ( 'NONE',  ( 1.545624935189822177E-15, 9.165435523385314198, -6.527800000000000047 ) ) ;
#14782=DIRECTION ( 'NONE',  ( 0.000000000000000000, 0.000000000000000000, -1.000000000000000000 ) ) ;
#14786=CARTESIAN_POINT ( 'NONE',  ( -4.644907831421410727, 6.483696736553158146, 4.577366046962239032E-15 ) ) ;
#14820=CARTESIAN_POINT ( 'NONE',  ( -1.300631254478304744, 8.414515718495824359, -0.3148715423363414589 ) ) ;
#14881=LINE ( 'NONE', #5757, #179 ) ;
#14896=CARTESIAN_POINT ( 'NONE',  ( 0.6476140635210377861, -8.791535369480467210, -0.4930775504667766485 ) ) ;
#14922=CARTESIAN_POINT ( 'NONE',  ( 4.762500000000000178, 5.832380380939270108E-16, -6.502399999999998847 ) ) ;
#14928=VECTOR ( 'NONE', #4333, 1000.000000000000000 ) ;
#14954=DIRECTION ( 'NONE',  ( -0.8191520442889917986, 0.000000000000000000, -0.5735764363510460484 ) ) ;
#14966=EDGE_LOOP ( 'NONE', ( #6431, #6331, #12423, #366 ) ) ;
#15010=FILL_AREA_STYLE ('',( #8906 ) ) ;
#15028=ADVANCED_FACE ( 'NONE', ( #3447, #6526 ), #12657, .T. ) ;
#15040=DIRECTION ( 'NONE',  ( -0.8660254037844383745, -0.5000000000000004441, 0.000000000000000000 ) ) ;
#15068=ADVANCED_FACE ( 'NONE', ( #246 ), #11249, .F. ) ;
#15071=ORIENTED_EDGE ( 'NONE', *, *, #6224, .T. ) ;
#15104=CIRCLE ( 'NONE', #17022, 7.937500000000000000 ) ;
#15154=ORIENTED_EDGE ( 'NONE', *, *, #2547, .F. ) ;
#15191=LINE ( 'NONE', #13483, #6384 ) ;
#15238=VECTOR ( 'NONE', #6272, 1000.000000000000114 ) ;
#15243=CARTESIAN_POINT ( 'NONE',  ( -7.937500000000000000, 4.582717761692651770, -6.527800000000000047 ) ) ;
#15273=DIRECTION ( 'NONE',  ( 1.000000000000000000, 0.000000000000000000, 0.000000000000000000 ) ) ;
#15280=VECTOR ( 'NONE', #10196, 1000.000000000000000 ) ;
#15284=DIRECTION ( 'NONE',  ( -1.000000000000000000, 0.000000000000000000, 0.000000000000000000 ) ) ;
#15365=PRODUCT_CONTEXT ( 'NONE', #12515, 'mechanical' ) ;
#15373=CONICAL_SURFACE ( 'NONE', #2563, 7.937500000000000000, 1.047197551196596521 ) ;
#15400=CARTESIAN_POINT ( 'NONE',  ( 7.937500000000001776, 3.090998114436798616, -0.3168978725525095075 ) ) ;
#15457=CARTESIAN_POINT ( 'NONE',  ( -7.937500000000000000, -4.582717761692662428, -6.527800000000000047 ) ) ;
#15476=AXIS2_PLACEMENT_3D ( 'NONE', #14048, #15556, #6232 ) ;
#15497=LINE ( 'NONE', #7974, #15238 ) ;
#15556=DIRECTION ( 'NONE',  ( -1.000000000000000000, 0.000000000000000000, 0.000000000000000000 ) ) ;
#15561=ORIENTED_EDGE ( 'NONE', *, *, #16385, .T. ) ;
#15563=FACE_OUTER_BOUND ( 'NONE', #9743, .T. ) ;
#15630=VERTEX_POINT ( 'NONE', #16133 ) ;
#15856=ADVANCED_FACE ( 'NONE', ( #3096 ), #15373, .T. ) ;
#15857=EDGE_LOOP ( 'NONE', ( #8213, #11819, #1577, #18322, #5868 ) ) ;
#15893=PLANE ( 'NONE',  #17744 ) ;
#15908=CIRCLE ( 'NONE', #18132, 7.937500000000000000 ) ;
#15933=CARTESIAN_POINT ( 'NONE',  ( 7.937500000000000000, -4.582717761692665981, -6.527800000000000047 ) ) ;
#16028=CARTESIAN_POINT ( 'NONE',  ( -3.968750000000004441, 6.874076642538978987, 0.000000000000000000 ) ) ;
#16056=DIRECTION ( 'NONE',  ( 1.000000000000000000, 0.000000000000000000, 0.000000000000000000 ) ) ;
#16087=ADVANCED_FACE ( 'NONE', ( #7333 ), #1580, .T. ) ;
#16133=CARTESIAN_POINT ( 'NONE',  ( 3.968750000000000000, 0.000000000000000000, -0.5557897334539606549 ) ) ;
#16148=CARTESIAN_POINT ( 'NONE',  ( 0.6492350739116989899, 8.790599478695050095, -0.4925372136696584136 ) ) ;
#16198=DIRECTION ( 'NONE',  ( -1.000000000000000000, 0.000000000000000000, 0.000000000000000000 ) ) ;
#16259=DIRECTION ( 'NONE',  ( -1.000000000000000000, 0.000000000000000000, 0.000000000000000000 ) ) ;
#16261=AXIS2_PLACEMENT_3D ( 'NONE', #9166, #2953, #15273 ) ;
#16266=PRODUCT_DEFINITION_FORMATION_WITH_SPECIFIED_SOURCE ( 'ANY', '', #12896, .NOT_KNOWN. ) ;
#16279=CARTESIAN_POINT ( 'NONE',  ( 7.937500000000000000, 0.000000000000000000, 0.000000000000000000 ) ) ;
#16288=CARTESIAN_POINT ( 'NONE',  ( 5.645569974854462103, 5.905964178674214082, -0.1296323192022580117 ) ) ;
#16294=ADVANCED_FACE ( 'NONE', ( #5822 ), #4431, .F. ) ;
#16309=ADVANCED_FACE ( 'NONE', ( #18338 ), #11838, .T. ) ;
#16330=VECTOR ( 'NONE', #14954, 1000.000000000000227 ) ;
#16345=DIRECTION ( 'NONE',  ( 0.000000000000000000, 0.000000000000000000, -1.000000000000000000 ) ) ;
#16346=DIRECTION ( 'NONE',  ( 0.5000000000000009992, 0.8660254037844380415, -0.000000000000000000 ) ) ;
#16385=EDGE_CURVE ( 'NONE', #3618, #4586, #2233, .T. ) ;
#16395=CONICAL_SURFACE ( 'NONE', #10337, 4.762500000000000178, 0.9599310885968813656 ) ;
#16451=DIRECTION ( 'NONE',  ( -0.000000000000000000, -0.000000000000000000, 1.000000000000000000 ) ) ;
#16472=ORIENTED_EDGE ( 'NONE', *, *, #17807, .T. ) ;
#16510=CARTESIAN_POINT ( 'NONE',  ( -7.937500000000000000, 4.582717761692651770, -0.7089489049740185234 ) ) ;
#16530=LINE ( 'NONE', #3111, #3072 ) ;
#16548=EDGE_CURVE ( 'NONE', #2502, #1264, #10225, .T. ) ;
#16589=CARTESIAN_POINT ( 'NONE',  ( -7.937500000000000000, 4.582717761692651770, -6.527800000000000047 ) ) ;
#16599=VERTEX_POINT ( 'NONE', #11617 ) ;
#16639=CARTESIAN_POINT ( 'NONE',  ( -3.968750000000007994, -6.874076642538976323, 0.000000000000000000 ) ) ;
#16650=FILL_AREA_STYLE ('',( #4536 ) ) ;
#16653=EDGE_CURVE ( 'NONE', #9186, #16599, #9844, .T. ) ;
#16674=EDGE_CURVE ( 'NONE', #9544, #12464, #6987, .T. ) ;
#16724=AXIS2_PLACEMENT_3D ( 'NONE', #17428, #9833, #6230 ) ;
#16745=CARTESIAN_POINT ( 'NONE',  ( 0.000000000000000000, 0.000000000000000000, -6.527800000000000047 ) ) ;
#16772=EDGE_LOOP ( 'NONE', ( #11714, #17386, #1967, #10587, #18125 ) ) ;
#16784=PRODUCT_DEFINITION ( 'UNKNOWN', '', #16266, #18800 ) ;
#16800=VECTOR ( 'NONE', #14399, 1000.000000000000000 ) ;
#16828=DIRECTION ( 'NONE',  ( 1.000000000000000000, 0.000000000000000000, 0.000000000000000000 ) ) ;
#16860=EDGE_LOOP ( 'NONE', ( #17552, #5625, #1005 ) ) ;
#16916=DIRECTION ( 'NONE',  ( 0.8660254037844383745, 0.5000000000000004441, 0.000000000000000000 ) ) ;
#16931=EDGE_CURVE ( 'NONE', #7032, #9186, #15191, .T. ) ;
#16957=EDGE_LOOP ( 'NONE', ( #13656, #14438, #15154, #12332, #5536, #9077 ) ) ;
#16996=CARTESIAN_POINT ( 'NONE',  ( 3.968750000000007994, 6.874076642538976323, 0.000000000000000000 ) ) ;
#17022=AXIS2_PLACEMENT_3D ( 'NONE', #956, #5453, #11563 ) ;
#17023=EDGE_LOOP ( 'NONE', ( #9437, #18859, #17876 ) ) ;
#17033=ORIENTED_EDGE ( 'NONE', *, *, #13590, .T. ) ;
#17115=CARTESIAN_POINT ( 'NONE',  ( 0.000000000000000000, 0.000000000000000000, -25.03750572909317285 ) ) ;
#17116=B_SPLINE_CURVE_WITH_KNOTS ( 'NONE', 3,
 ( #19602, #5983, #8805, #4695, #19699, #16510 ),
 .UNSPECIFIED., .F., .F.,
 ( 4, 2, 4 ),
 ( 0.01281224986012821296, 0.01513166665602954861, 0.01745108345193088425 ),
 .UNSPECIFIED. ) ;
#17185=VECTOR ( 'NONE', #699, 1000.000000000000000 ) ;
#17276=DIRECTION ( 'NONE',  ( -0.000000000000000000, -0.000000000000000000, -1.000000000000000000 ) ) ;
#17344=ADVANCED_FACE ( 'NONE', ( #7076 ), #13764, .T. ) ;
#17362=CARTESIAN_POINT ( 'NONE',  ( 7.937499999999996447, -4.582717761692668645, -0.7089489049740167470 ) ) ;
#17386=ORIENTED_EDGE ( 'NONE', *, *, #18223, .T. ) ;
#17428=CARTESIAN_POINT ( 'NONE',  ( 0.000000000000000000, 0.000000000000000000, 0.000000000000000000 ) ) ;
#17459=CYLINDRICAL_SURFACE ( 'NONE', #8724, 3.968750000000000000 ) ;
#17497=CARTESIAN_POINT ( 'NONE',  ( 7.937500000000000000, -3.073999505363504081, -0.3133235625263147694 ) ) ;
#17515=CARTESIAN_POINT ( 'NONE',  ( 0.000000000000000000, 0.000000000000000000, 0.000000000000000000 ) ) ;
#17552=ORIENTED_EDGE ( 'NONE', *, *, #883, .T. ) ;
#17578=VECTOR ( 'NONE', #2216, 1000.000000000000000 ) ;
#17627=CARTESIAN_POINT ( 'NONE',  ( -2.291930025145539673, 7.842189106403748333, -0.1296323192022596493 ) ) ;
#17661=EDGE_CURVE ( 'NONE', #5161, #11518, #4593, .T. ) ;
#17698=CARTESIAN_POINT ( 'NONE',  ( 2.291930025145539229, -7.842189106403761656, -0.1296323192022672544 ) ) ;
#17725=DIRECTION ( 'NONE',  ( -1.000000000000000000, 0.000000000000000000, 0.000000000000000000 ) ) ;
#17737=CARTESIAN_POINT ( 'NONE',  ( -7.937500000000000000, -0.7744039358429345432, 6.268043809681820044E-17 ) ) ;
#17744=AXIS2_PLACEMENT_3D ( 'NONE', #18887, #9701, #489 ) ;
#17762=DIRECTION ( 'NONE',  ( -1.000000000000000000, 0.000000000000000000, 0.000000000000000000 ) ) ;
#17795=UNCERTAINTY_MEASURE_WITH_UNIT (LENGTH_MEASURE( 1.000000000000000082E-05 ), #9346, 'distance_accuracy_value', 'NONE');
#17805=ORIENTED_EDGE ( 'NONE', *, *, #2864, .F. ) ;
#17807=EDGE_CURVE ( 'NONE', #201, #5154, #8753, .T. ) ;
#17822=CARTESIAN_POINT ( 'NONE',  ( 4.762500000000000178, 0.000000000000000000, -6.527800000000000047 ) ) ;
#17867=ORIENTED_EDGE ( 'NONE', *, *, #6685, .T. ) ;
#17876=ORIENTED_EDGE ( 'NONE', *, *, #1237, .F. ) ;
#17881=EDGE_CURVE ( 'NONE', #4586, #5154, #1641, .T. ) ;
#18006=EDGE_CURVE ( 'NONE', #7032, #11518, #550, .T. ) ;
#18020=( LENGTH_UNIT ( ) NAMED_UNIT ( * ) SI_UNIT ( .MILLI., .METRE. ) );
#18084=CARTESIAN_POINT ( 'NONE',  ( -6.634287453978999771, 5.335127875949178033, -0.3142460757452209541 ) ) ;
#18098=EDGE_LOOP ( 'NONE', ( #13852, #9990, #14062, #18576 ) ) ;
#18119=EDGE_LOOP ( 'NONE', ( #820, #614, #19247 ) ) ;
#18125=ORIENTED_EDGE ( 'NONE', *, *, #10432, .T. ) ;
#18126=CARTESIAN_POINT ( 'NONE',  ( -1.001543065824775120E-15, -9.165435523385328409, -6.527800000000000047 ) ) ;
#18132=AXIS2_PLACEMENT_3D ( 'NONE', #7125, #2349, #13342 ) ;
#18171=CARTESIAN_POINT ( 'NONE',  ( 0.000000000000000000, 0.000000000000000000, 0.000000000000000000 ) ) ;
#18223=EDGE_CURVE ( 'NONE', #12464, #8660, #11967, .T. ) ;
#18297=DIRECTION ( 'NONE',  ( 0.000000000000000000, 0.000000000000000000, 1.000000000000000000 ) ) ;
#18319=FACE_OUTER_BOUND ( 'NONE', #7871, .T. ) ;
#18322=ORIENTED_EDGE ( 'NONE', *, *, #14086, .F. ) ;
#18338=FACE_OUTER_BOUND ( 'NONE', #1531, .T. ) ;
#18350=VECTOR ( 'NONE', #18525, 1000.000000000000000 ) ;
#18373=( GEOMETRIC_REPRESENTATION_CONTEXT ( 3 ) GLOBAL_UNCERTAINTY_ASSIGNED_CONTEXT ( ( #17795 ) ) GLOBAL_UNIT_ASSIGNED_CONTEXT ( ( #9346, #9148, #1542 ) ) REPRESENTATION_CONTEXT ( 'NONE', 'WORKASPACE' ) );
#18382=DIRECTION ( 'NONE',  ( 1.000000000000000000, -1.776356839400250465E-15, 0.000000000000000000 ) ) ;
#18393=DIRECTION ( 'NONE',  ( 1.000000000000000000, 0.000000000000000000, -0.000000000000000000 ) ) ;
#18398=EDGE_CURVE ( 'NONE', #1264, #3846, #12521, .T. ) ;
#18451=VERTEX_POINT ( 'NONE', #11324 ) ;
#18493=CARTESIAN_POINT ( 'NONE',  ( 7.937500000000000000, 4.582717761692664205, -0.7089489049740167470 ) ) ;
#18503=CARTESIAN_POINT ( 'NONE',  ( 0.000000000000000000, 0.000000000000000000, 0.000000000000000000 ) ) ;
#18525=DIRECTION ( 'NONE',  ( 0.8660254037844380415, -0.5000000000000009992, 0.000000000000000000 ) ) ;
#18576=ORIENTED_EDGE ( 'NONE', *, *, #9986, .F. ) ;
#18650=ORIENTED_EDGE ( 'NONE', *, *, #2202, .F. ) ;
#18681=ORIENTED_EDGE ( 'NONE', *, *, #13470, .T. ) ;
#18692=AXIS2_PLACEMENT_3D ( 'NONE', #7051, #14782, #7248 ) ;
#18754=ORIENTED_EDGE ( 'NONE', *, *, #17881, .T. ) ;
#18760=EDGE_CURVE ( 'NONE', #4468, #1215, #17116, .T. ) ;
#18769=CARTESIAN_POINT ( 'NONE',  ( 4.762500000000000178, 5.832380380939270108E-16, -6.502399999999998847 ) ) ;
#18800=PRODUCT_DEFINITION_CONTEXT ( 'detailed design', #13915, 'design' ) ;
#18826=VECTOR ( 'NONE', #4645, 1000.000000000000000 ) ;
#18859=ORIENTED_EDGE ( 'NONE', *, *, #17661, .T. ) ;
#18868=CARTESIAN_POINT ( 'NONE',  ( 0.000000000000000000, 0.000000000000000000, 0.000000000000000000 ) ) ;
#18881=CARTESIAN_POINT ( 'NONE',  ( -7.937500000000000000, -4.582717761692664205, -0.7089489049740167470 ) ) ;
#18887=CARTESIAN_POINT ( 'NONE',  ( -7.937500000000000000, -4.582717761692662428, -6.527800000000000047 ) ) ;
#18941=CARTESIAN_POINT ( 'NONE',  ( 0.000000000000000000, 0.000000000000000000, -6.502399999999998847 ) ) ;
#19028=DIRECTION ( 'NONE',  ( 0.000000000000000000, 0.000000000000000000, 1.000000000000000000 ) ) ;
#19040=CARTESIAN_POINT ( 'NONE',  ( 3.292592168578600820, 7.264456548524799828, 4.858580985450665956E-15 ) ) ;
#19085=CARTESIAN_POINT ( 'NONE',  ( -7.937500000000000000, 4.582717761692651770, -0.7089489049740185234 ) ) ;
#19123=CARTESIAN_POINT ( 'NONE',  ( -3.293609449816390367, 7.263869220928322434, -0.01675691374232982436 ) ) ;
#19159=FACE_OUTER_BOUND ( 'NONE', #7768, .T. ) ;
#19169=AXIS2_PLACEMENT_3D ( 'NONE', #7411, #9139, #15040 ) ;
#19179=CARTESIAN_POINT ( 'NONE',  ( 3.968750000000007994, 6.874076642538976323, 0.000000000000000000 ) ) ;
#19192=AXIS2_PLACEMENT_3D ( 'NONE', #17515, #5203, #3901 ) ;
#19202=DIRECTION ( 'NONE',  ( -0.000000000000000000, -0.000000000000000000, -1.000000000000000000 ) ) ;
#19232=CARTESIAN_POINT ( 'NONE',  ( -7.937500000000000000, -4.582717761692664205, -0.7089489049740167470 ) ) ;
#19239=CARTESIAN_POINT ( 'NONE',  ( 0.000000000000000000, 0.000000000000000000, -6.527800000000000047 ) ) ;
#19247=ORIENTED_EDGE ( 'NONE', *, *, #13470, .F. ) ;
#19250=DIRECTION ( 'NONE',  ( -0.000000000000000000, -0.000000000000000000, 1.000000000000000000 ) ) ;
#19257=EDGE_LOOP ( 'NONE', ( #7285, #4768 ) ) ;
#19271=AXIS2_PLACEMENT_3D ( 'NONE', #14220, #314, #14117 ) ;
#19334=CIRCLE ( 'NONE', #18692, 3.968750000000000000 ) ;
#19340=CARTESIAN_POINT ( 'NONE',  ( 0.000000000000000000, 0.000000000000000000, -0.5557897334539606549 ) ) ;
#19389=AXIS2_PLACEMENT_3D ( 'NONE', #5063, #475, #12873 ) ;
#19437=EDGE_CURVE ( 'NONE', #5161, #8660, #15104, .T. ) ;
#19440=DIRECTION ( 'NONE',  ( -0.8660254037844380415, 0.5000000000000009992, 0.000000000000000000 ) ) ;
#19529=CARTESIAN_POINT ( 'NONE',  ( 0.000000000000000000, 0.000000000000000000, -6.527800000000000047 ) ) ;
#19530=CARTESIAN_POINT ( 'NONE',  ( 1.545624935189822177E-15, 9.165435523385314198, -6.527800000000000047 ) ) ;
#19554=DIRECTION ( 'NONE',  ( -1.000000000000000000, 0.000000000000000000, 0.000000000000000000 ) ) ;
#19569=ADVANCED_FACE ( 'NONE', ( #12773 ), #5525, .T. ) ;
#19571=CLOSED_SHELL ( 'NONE', ( #13345, #368, #2448, #16294, #2966, #16309, #10185, #15068, #12467, #9714, #3597, #15028, #8712, #15856, #1490, #16087, #19569, #14041, #17344, #14573, #679, #7143 ) ) ;
#19590=CARTESIAN_POINT ( 'NONE',  ( 3.968750000000004441, -6.874076642538978987, 0.000000000000000000 ) ) ;
#19597=COLOUR_RGB ( '', 0.66274510, 0.83137255, 0.94901961) ;
#19601=CIRCLE ( 'NONE', #7120, 7.937500000000000000 ) ;
#19602=CARTESIAN_POINT ( 'NONE',  ( -7.937500000000000000, 0.000000000000000000, 0.000000000000000000 ) ) ;
#19643=CIRCLE ( 'NONE', #13890, 3.968750000000000000 ) ;
#19658=EDGE_LOOP ( 'NONE', ( #9931, #8050, #7809 ) ) ;
#19668=VECTOR ( 'NONE', #8032, 1000.000000000000000 ) ;
#19673=ORIENTED_EDGE ( 'NONE', *, *, #16674, .T. ) ;
#19699=CARTESIAN_POINT ( 'NONE',  ( -7.937500000000000000, 3.841717848563040771, -0.4950406553165774826 ) ) ;
#19739=ORIENTED_EDGE ( 'NONE', *, *, #17881, .F. ) ;
#19745=ADVANCED_BREP_SHAPE_REPRESENTATION ( '', ( #9397, #16724 ), #5229 ) ;
#19774=CARTESIAN_POINT ( 'NONE',  ( 0.000000000000000000, 0.000000000000000000, -0.6113687067993561763 ) ) ;
ENDSEC;
END-ISO-10303-21;
